ISO-10303-21;
HEADER;
/* Generated by software containing ST-Developer
 * from STEP Tools, Inc. (www.steptools.com) 
 */

FILE_DESCRIPTION(
/* description */ ('PAT-072'),
/* implementation_level */ '2;1');

FILE_NAME(
/* name */ 'M2 sight screw.step',
/* time_stamp */ '2026-10-29T20:11:56-07:00',
/* author */ (''),
/* organization */ (''),
/* preprocessor_version */ 'ST-DEVELOPER v20.2',
/* originating_system */ 'Autodesk Translation Framework v15.17.0.0',
/* authorisation */ '');

FILE_SCHEMA (('AUTOMOTIVE_DESIGN { 1 0 10303 214 3 1 1 }'));
ENDSEC;

DATA;
#10=MECHANICAL_DESIGN_GEOMETRIC_PRESENTATION_REPRESENTATION('',(#354),#11432);
#282=SHAPE_REPRESENTATION_RELATIONSHIP('SRR','None',#11586,#318);
#318=ADVANCED_BREP_SHAPE_REPRESENTATION('',(#390),#11417);
#354=STYLED_ITEM('',(#11826),#390);
#390=MANIFOLD_SOLID_BREP('Body1',#6089);
#528=FACE_BOUND('',#1531,.T.);
#702=PLANE('',#6953);
#703=PLANE('',#6954);
#704=PLANE('',#6955);
#705=PLANE('',#6958);
#706=PLANE('',#6960);
#707=PLANE('',#6963);
#708=PLANE('',#6969);
#1027=FACE_OUTER_BOUND('',#1525,.T.);
#1028=FACE_OUTER_BOUND('',#1526,.T.);
#1029=FACE_OUTER_BOUND('',#1527,.T.);
#1030=FACE_OUTER_BOUND('',#1528,.T.);
#1031=FACE_OUTER_BOUND('',#1529,.T.);
#1032=FACE_OUTER_BOUND('',#1530,.T.);
#1033=FACE_OUTER_BOUND('',#1532,.T.);
#1034=FACE_OUTER_BOUND('',#1533,.T.);
#1035=FACE_OUTER_BOUND('',#1534,.T.);
#1525=EDGE_LOOP('',(#5006,#5007,#5008,#5009));
#1526=EDGE_LOOP('',(#5010,#5011,#5012,#5013));
#1527=EDGE_LOOP('',(#5014,#5015,#5016,#5017));
#1528=EDGE_LOOP('',(#5018,#5019));
#1529=EDGE_LOOP('',(#5020,#5021,#5022));
#1530=EDGE_LOOP('',(#5023));
#1531=EDGE_LOOP('',(#5024));
#1532=EDGE_LOOP('',(#5025,#5026,#5027,#5028,#5029,#5030,#5031,#5032,#5033,
#5034,#5035,#5036));
#1533=EDGE_LOOP('',(#5037,#5038,#5039,#5040));
#1534=EDGE_LOOP('',(#5041));
#1952=LINE('',#10696,#2371);
#1953=LINE('',#10698,#2372);
#1954=LINE('',#10700,#2373);
#1955=LINE('',#10701,#2374);
#1956=LINE('',#10705,#2375);
#1957=LINE('',#10707,#2376);
#1958=LINE('',#10709,#2377);
#1959=LINE('',#10710,#2378);
#1960=LINE('',#10726,#2379);
#1961=LINE('',#10730,#2380);
#2371=VECTOR('',#8407,1.);
#2372=VECTOR('',#8408,1.);
#2373=VECTOR('',#8409,1.);
#2374=VECTOR('',#8410,1.);
#2375=VECTOR('',#8413,1.);
#2376=VECTOR('',#8414,1.);
#2377=VECTOR('',#8415,1.);
#2378=VECTOR('',#8416,1.);
#2379=VECTOR('',#8441,0.175);
#2380=VECTOR('',#8446,0.1);
#2735=CIRCLE('',#6956,0.175);
#2736=CIRCLE('',#6957,0.175);
#2737=CIRCLE('',#6959,0.175);
#2738=CIRCLE('',#6961,0.175);
#2739=CIRCLE('',#6962,0.175);
#2740=CIRCLE('',#6964,0.175);
#2741=CIRCLE('',#6965,0.1);
#2742=CIRCLE('',#6968,0.1);
#3142=VERTEX_POINT('',#10694);
#3143=VERTEX_POINT('',#10695);
#3144=VERTEX_POINT('',#10697);
#3145=VERTEX_POINT('',#10699);
#3146=VERTEX_POINT('',#10703);
#3147=VERTEX_POINT('',#10704);
#3148=VERTEX_POINT('',#10706);
#3149=VERTEX_POINT('',#10708);
#3150=VERTEX_POINT('',#10717);
#3151=VERTEX_POINT('',#10721);
#3152=VERTEX_POINT('',#10723);
#3153=VERTEX_POINT('',#10728);
#3792=EDGE_CURVE('',#3142,#3143,#1952,.T.);
#3793=EDGE_CURVE('',#3142,#3144,#1953,.T.);
#3794=EDGE_CURVE('',#3145,#3144,#1954,.T.);
#3795=EDGE_CURVE('',#3143,#3145,#1955,.T.);
#3796=EDGE_CURVE('',#3146,#3147,#1956,.T.);
#3797=EDGE_CURVE('',#3148,#3146,#1957,.T.);
#3798=EDGE_CURVE('',#3149,#3148,#1958,.T.);
#3799=EDGE_CURVE('',#3149,#3147,#1959,.T.);
#3800=EDGE_CURVE('',#3147,#3142,#2735,.T.);
#3801=EDGE_CURVE('',#3144,#3149,#2736,.T.);
#3802=EDGE_CURVE('',#3148,#3146,#2737,.T.);
#3803=EDGE_CURVE('',#3150,#3145,#2738,.T.);
#3804=EDGE_CURVE('',#3143,#3150,#2739,.T.);
#3805=EDGE_CURVE('',#3151,#3151,#2740,.T.);
#3806=EDGE_CURVE('',#3152,#3152,#2741,.T.);
#3807=EDGE_CURVE('',#3151,#3150,#1960,.T.);
#3808=EDGE_CURVE('',#3153,#3153,#2742,.T.);
#3809=EDGE_CURVE('',#3153,#3152,#1961,.T.);
#5006=ORIENTED_EDGE('',*,*,#3792,.F.);
#5007=ORIENTED_EDGE('',*,*,#3793,.T.);
#5008=ORIENTED_EDGE('',*,*,#3794,.F.);
#5009=ORIENTED_EDGE('',*,*,#3795,.F.);
#5010=ORIENTED_EDGE('',*,*,#3796,.F.);
#5011=ORIENTED_EDGE('',*,*,#3797,.F.);
#5012=ORIENTED_EDGE('',*,*,#3798,.F.);
#5013=ORIENTED_EDGE('',*,*,#3799,.T.);
#5014=ORIENTED_EDGE('',*,*,#3800,.F.);
#5015=ORIENTED_EDGE('',*,*,#3799,.F.);
#5016=ORIENTED_EDGE('',*,*,#3801,.F.);
#5017=ORIENTED_EDGE('',*,*,#3793,.F.);
#5018=ORIENTED_EDGE('',*,*,#3797,.T.);
#5019=ORIENTED_EDGE('',*,*,#3802,.F.);
#5020=ORIENTED_EDGE('',*,*,#3795,.T.);
#5021=ORIENTED_EDGE('',*,*,#3803,.F.);
#5022=ORIENTED_EDGE('',*,*,#3804,.F.);
#5023=ORIENTED_EDGE('',*,*,#3805,.T.);
#5024=ORIENTED_EDGE('',*,*,#3806,.F.);
#5025=ORIENTED_EDGE('',*,*,#3805,.F.);
#5026=ORIENTED_EDGE('',*,*,#3807,.T.);
#5027=ORIENTED_EDGE('',*,*,#3803,.T.);
#5028=ORIENTED_EDGE('',*,*,#3794,.T.);
#5029=ORIENTED_EDGE('',*,*,#3801,.T.);
#5030=ORIENTED_EDGE('',*,*,#3798,.T.);
#5031=ORIENTED_EDGE('',*,*,#3802,.T.);
#5032=ORIENTED_EDGE('',*,*,#3796,.T.);
#5033=ORIENTED_EDGE('',*,*,#3800,.T.);
#5034=ORIENTED_EDGE('',*,*,#3792,.T.);
#5035=ORIENTED_EDGE('',*,*,#3804,.T.);
#5036=ORIENTED_EDGE('',*,*,#3807,.F.);
#5037=ORIENTED_EDGE('',*,*,#3808,.F.);
#5038=ORIENTED_EDGE('',*,*,#3809,.T.);
#5039=ORIENTED_EDGE('',*,*,#3806,.T.);
#5040=ORIENTED_EDGE('',*,*,#3809,.F.);
#5041=ORIENTED_EDGE('',*,*,#3808,.T.);
#5657=CYLINDRICAL_SURFACE('',#6966,0.175);
#5658=CYLINDRICAL_SURFACE('',#6967,0.1);
#5926=ADVANCED_FACE('',(#1027),#702,.F.);
#5927=ADVANCED_FACE('',(#1028),#703,.F.);
#5928=ADVANCED_FACE('',(#1029),#704,.F.);
#5929=ADVANCED_FACE('',(#1030),#705,.F.);
#5930=ADVANCED_FACE('',(#1031),#706,.F.);
#5931=ADVANCED_FACE('',(#1032,#528),#707,.T.);
#5932=ADVANCED_FACE('',(#1033),#5657,.T.);
#5933=ADVANCED_FACE('',(#1034),#5658,.T.);
#5934=ADVANCED_FACE('',(#1035),#708,.T.);
#6089=CLOSED_SHELL('',(#5926,#5927,#5928,#5929,#5930,#5931,#5932,#5933,
#5934));
#6952=AXIS2_PLACEMENT_3D('',#10692,#8403,#8404);
#6953=AXIS2_PLACEMENT_3D('',#10693,#8405,#8406);
#6954=AXIS2_PLACEMENT_3D('',#10702,#8411,#8412);
#6955=AXIS2_PLACEMENT_3D('',#10711,#8417,#8418);
#6956=AXIS2_PLACEMENT_3D('',#10712,#8419,#8420);
#6957=AXIS2_PLACEMENT_3D('',#10713,#8421,#8422);
#6958=AXIS2_PLACEMENT_3D('',#10714,#8423,#8424);
#6959=AXIS2_PLACEMENT_3D('',#10715,#8425,#8426);
#6960=AXIS2_PLACEMENT_3D('',#10716,#8427,#8428);
#6961=AXIS2_PLACEMENT_3D('',#10718,#8429,#8430);
#6962=AXIS2_PLACEMENT_3D('',#10719,#8431,#8432);
#6963=AXIS2_PLACEMENT_3D('',#10720,#8433,#8434);
#6964=AXIS2_PLACEMENT_3D('',#10722,#8435,#8436);
#6965=AXIS2_PLACEMENT_3D('',#10724,#8437,#8438);
#6966=AXIS2_PLACEMENT_3D('',#10725,#8439,#8440);
#6967=AXIS2_PLACEMENT_3D('',#10727,#8442,#8443);
#6968=AXIS2_PLACEMENT_3D('',#10729,#8444,#8445);
#6969=AXIS2_PLACEMENT_3D('',#10731,#8447,#8448);
#8403=DIRECTION('axis',(0.,0.,1.));
#8404=DIRECTION('refdir',(1.,0.,0.));
#8405=DIRECTION('center_axis',(-1.,0.,0.));
#8406=DIRECTION('ref_axis',(0.,0.,1.));
#8407=DIRECTION('',(0.,-1.,0.));
#8408=DIRECTION('',(0.,0.,1.));
#8409=DIRECTION('',(0.,1.,0.));
#8410=DIRECTION('',(0.,0.,1.));
#8411=DIRECTION('center_axis',(1.,0.,0.));
#8412=DIRECTION('ref_axis',(0.,0.,-1.));
#8413=DIRECTION('',(0.,1.,0.));
#8414=DIRECTION('',(0.,0.,-1.));
#8415=DIRECTION('',(0.,-1.,0.));
#8416=DIRECTION('',(0.,0.,-1.));
#8417=DIRECTION('center_axis',(0.,1.,0.));
#8418=DIRECTION('ref_axis',(0.,0.,1.));
#8419=DIRECTION('center_axis',(0.,1.,0.));
#8420=DIRECTION('ref_axis',(1.,0.,0.));
#8421=DIRECTION('center_axis',(0.,1.,0.));
#8422=DIRECTION('ref_axis',(1.,0.,0.));
#8423=DIRECTION('center_axis',(0.,1.,0.));
#8424=DIRECTION('ref_axis',(1.,0.,0.));
#8425=DIRECTION('center_axis',(0.,1.,0.));
#8426=DIRECTION('ref_axis',(1.,0.,0.));
#8427=DIRECTION('center_axis',(0.,1.,0.));
#8428=DIRECTION('ref_axis',(1.,0.,0.));
#8429=DIRECTION('center_axis',(0.,1.,0.));
#8430=DIRECTION('ref_axis',(1.,0.,0.));
#8431=DIRECTION('center_axis',(0.,1.,0.));
#8432=DIRECTION('ref_axis',(1.,0.,0.));
#8433=DIRECTION('center_axis',(0.,1.,0.));
#8434=DIRECTION('ref_axis',(1.,0.,0.));
#8435=DIRECTION('center_axis',(0.,1.,0.));
#8436=DIRECTION('ref_axis',(1.,0.,0.));
#8437=DIRECTION('center_axis',(0.,1.,0.));
#8438=DIRECTION('ref_axis',(1.,0.,0.));
#8439=DIRECTION('center_axis',(0.,1.,0.));
#8440=DIRECTION('ref_axis',(1.,0.,0.));
#8441=DIRECTION('',(0.,-1.,0.));
#8442=DIRECTION('center_axis',(0.,1.,0.));
#8443=DIRECTION('ref_axis',(1.,0.,0.));
#8444=DIRECTION('center_axis',(0.,1.,0.));
#8445=DIRECTION('ref_axis',(1.,0.,0.));
#8446=DIRECTION('',(0.,-1.,0.));
#8447=DIRECTION('center_axis',(0.,1.,0.));
#8448=DIRECTION('ref_axis',(1.,0.,0.));
#10692=CARTESIAN_POINT('',(0.,0.,0.));
#10693=CARTESIAN_POINT('Origin',(-0.83,-3.4,9.6));
#10694=CARTESIAN_POINT('',(-0.83,-3.2,9.62759060350433));
#10695=CARTESIAN_POINT('',(-0.83,-3.3,9.62759060350433));
#10696=CARTESIAN_POINT('',(-0.83,-3.3,9.62759060350433));
#10697=CARTESIAN_POINT('',(-0.83,-3.2,9.97240939649567));
#10698=CARTESIAN_POINT('',(-0.83,-3.2,10.));
#10699=CARTESIAN_POINT('',(-0.83,-3.3,9.97240939649567));
#10700=CARTESIAN_POINT('',(-0.83,-3.3,9.97240939649567));
#10701=CARTESIAN_POINT('',(-0.83,-3.3,9.7));
#10702=CARTESIAN_POINT('Origin',(-0.77,-3.4,10.));
#10703=CARTESIAN_POINT('',(-0.77,-3.3,9.62759060350433));
#10704=CARTESIAN_POINT('',(-0.77,-3.2,9.62759060350433));
#10705=CARTESIAN_POINT('',(-0.77,-3.3,9.62759060350433));
#10706=CARTESIAN_POINT('',(-0.77,-3.3,9.97240939649567));
#10707=CARTESIAN_POINT('',(-0.77,-3.3,9.9));
#10708=CARTESIAN_POINT('',(-0.77,-3.2,9.97240939649567));
#10709=CARTESIAN_POINT('',(-0.77,-3.3,9.97240939649567));
#10710=CARTESIAN_POINT('',(-0.77,-3.2,9.6));
#10711=CARTESIAN_POINT('Origin',(-0.8,-3.2,9.8));
#10712=CARTESIAN_POINT('Origin',(-0.8,-3.2,9.8));
#10713=CARTESIAN_POINT('Origin',(-0.8,-3.2,9.8));
#10714=CARTESIAN_POINT('Origin',(-0.8,-3.3,9.8));
#10715=CARTESIAN_POINT('Origin',(-0.8,-3.3,9.8));
#10716=CARTESIAN_POINT('Origin',(-0.8,-3.3,9.8));
#10717=CARTESIAN_POINT('',(-0.975,-3.3,9.8));
#10718=CARTESIAN_POINT('Origin',(-0.8,-3.3,9.8));
#10719=CARTESIAN_POINT('Origin',(-0.8,-3.3,9.8));
#10720=CARTESIAN_POINT('Origin',(-0.8,-3.1,9.8));
#10721=CARTESIAN_POINT('',(-0.975,-3.1,9.8));
#10722=CARTESIAN_POINT('Origin',(-0.8,-3.1,9.8));
#10723=CARTESIAN_POINT('',(-0.9,-3.1,9.8));
#10724=CARTESIAN_POINT('Origin',(-0.8,-3.1,9.8));
#10725=CARTESIAN_POINT('Origin',(-0.8,-3.3,9.8));
#10726=CARTESIAN_POINT('',(-0.975,-3.3,9.8));
#10727=CARTESIAN_POINT('Origin',(-0.8,-3.1,9.8));
#10728=CARTESIAN_POINT('',(-0.9,-2.1,9.8));
#10729=CARTESIAN_POINT('Origin',(-0.8,-2.1,9.8));
#10730=CARTESIAN_POINT('',(-0.9,-3.1,9.8));
#10731=CARTESIAN_POINT('Origin',(-0.8,-2.1,9.8));
#11378=UNCERTAINTY_MEASURE_WITH_UNIT(LENGTH_MEASURE(0.001),#11433,
'DISTANCE_ACCURACY_VALUE',
'Maximum model space distance between geometric entities at asserted c
onnectivities');
#11393=UNCERTAINTY_MEASURE_WITH_UNIT(LENGTH_MEASURE(0.001),#11433,
'DISTANCE_ACCURACY_VALUE',
'Maximum model space distance between geometric entities at asserted c
onnectivities');
#11417=(
GEOMETRIC_REPRESENTATION_CONTEXT(3)
GLOBAL_UNCERTAINTY_ASSIGNED_CONTEXT((#11378))
GLOBAL_UNIT_ASSIGNED_CONTEXT((#11433,#11435,#11436))
REPRESENTATION_CONTEXT('','3D')
);
#11432=(
GEOMETRIC_REPRESENTATION_CONTEXT(3)
GLOBAL_UNCERTAINTY_ASSIGNED_CONTEXT((#11393))
GLOBAL_UNIT_ASSIGNED_CONTEXT((#11433,#11435,#11436))
REPRESENTATION_CONTEXT('','3D')
);
#11433=(
LENGTH_UNIT()
NAMED_UNIT(*)
SI_UNIT(.CENTI.,.METRE.)
);
#11435=(
NAMED_UNIT(*)
PLANE_ANGLE_UNIT()
SI_UNIT($,.RADIAN.)
);
#11436=(
NAMED_UNIT(*)
SI_UNIT($,.STERADIAN.)
SOLID_ANGLE_UNIT()
);
#11460=SHAPE_DEFINITION_REPRESENTATION(#11498,#11586);
#11498=PRODUCT_DEFINITION_SHAPE('',$,#11625);
#11586=SHAPE_REPRESENTATION('',(#6952),#11417);
#11601=PRODUCT_DEFINITION_CONTEXT('part definition',#11717,'design');
#11625=PRODUCT_DEFINITION('M2 sight screw','M2 sight screw',#11663,
#11601);
#11663=PRODUCT_DEFINITION_FORMATION('',$,#11742);
#11717=APPLICATION_CONTEXT(
'Core Data for Automotive Mechanical Design Process');
#11718=PRODUCT_CONTEXT('part definition',#11717,'mechanical');
#11742=PRODUCT('M2 sight screw','M2 sight screw',
'M2 sight screw',(#11718));
#11820=COLOUR_RGB('Black',0.12,0.14,0.17);
#11821=FILL_AREA_STYLE_COLOUR('',#11820);
#11822=FILL_AREA_STYLE('',(#11821));
#11823=SURFACE_STYLE_FILL_AREA(#11822);
#11824=SURFACE_SIDE_STYLE('',(#11823));
#11825=SURFACE_STYLE_USAGE(.BOTH.,#11824);
#11826=PRESENTATION_STYLE_ASSIGNMENT((#11825));
ENDSEC;
END-ISO-10303-21;
